ISO-10303-21;
HEADER;
/* Generated by software containing ST-Developer
 * from STEP Tools, Inc. (www.steptools.com) 
 */

FILE_DESCRIPTION(
/* description */ ('Bin tilter linkage'),
/* implementation_level */ '2;1');

FILE_NAME(
/* name */ 'M4 short cap screw (26).step',
/* time_stamp */ '2026-10-28T03:26:24-07:00',
/* author */ (''),
/* organization */ (''),
/* preprocessor_version */ 'ST-DEVELOPER v20.2',
/* originating_system */ 'Autodesk Translation Framework v15.17.0.0',
/* authorisation */ '');

FILE_SCHEMA (('AUTOMOTIVE_DESIGN { 1 0 10303 214 3 1 1 }'));
ENDSEC;

DATA;
#10=MECHANICAL_DESIGN_GEOMETRIC_PRESENTATION_REPRESENTATION('',(#927),#23728);
#715=SHAPE_REPRESENTATION_RELATIONSHIP('SRR','None',#24181,#821);
#821=ADVANCED_BREP_SHAPE_REPRESENTATION('',(#1040),#23681);
#927=STYLED_ITEM('',(#24772),#1040);
#1040=MANIFOLD_SOLID_BREP('Body1',#12458);
#1370=FACE_BOUND('',#3418,.T.);
#1717=PLANE('',#14693);
#1718=PLANE('',#14698);
#1719=PLANE('',#14701);
#2357=FACE_OUTER_BOUND('',#3417,.T.);
#2358=FACE_OUTER_BOUND('',#3419,.T.);
#2359=FACE_OUTER_BOUND('',#3420,.T.);
#2360=FACE_OUTER_BOUND('',#3421,.T.);
#2361=FACE_OUTER_BOUND('',#3422,.T.);
#3417=EDGE_LOOP('',(#10105));
#3418=EDGE_LOOP('',(#10106));
#3419=EDGE_LOOP('',(#10107,#10108,#10109,#10110));
#3420=EDGE_LOOP('',(#10111));
#3421=EDGE_LOOP('',(#10112,#10113,#10114,#10115));
#3422=EDGE_LOOP('',(#10116));
#4235=LINE('',#21731,#4910);
#4236=LINE('',#21737,#4911);
#4910=VECTOR('',#17902,0.350000000000001);
#4911=VECTOR('',#17911,0.199999999999999);
#5679=CIRCLE('',#14694,0.350000000000001);
#5680=CIRCLE('',#14695,0.199999999999999);
#5681=CIRCLE('',#14697,0.350000000000001);
#5682=CIRCLE('',#14700,0.199999999999999);
#6533=VERTEX_POINT('',#21725);
#6534=VERTEX_POINT('',#21727);
#6535=VERTEX_POINT('',#21730);
#6536=VERTEX_POINT('',#21735);
#7792=EDGE_CURVE('',#6533,#6533,#5679,.T.);
#7793=EDGE_CURVE('',#6534,#6534,#5680,.T.);
#7794=EDGE_CURVE('',#6533,#6535,#4235,.T.);
#7795=EDGE_CURVE('',#6535,#6535,#5681,.T.);
#7796=EDGE_CURVE('',#6536,#6536,#5682,.T.);
#7797=EDGE_CURVE('',#6536,#6534,#4236,.T.);
#10105=ORIENTED_EDGE('',*,*,#7792,.T.);
#10106=ORIENTED_EDGE('',*,*,#7793,.F.);
#10107=ORIENTED_EDGE('',*,*,#7792,.F.);
#10108=ORIENTED_EDGE('',*,*,#7794,.T.);
#10109=ORIENTED_EDGE('',*,*,#7795,.T.);
#10110=ORIENTED_EDGE('',*,*,#7794,.F.);
#10111=ORIENTED_EDGE('',*,*,#7795,.F.);
#10112=ORIENTED_EDGE('',*,*,#7796,.F.);
#10113=ORIENTED_EDGE('',*,*,#7797,.T.);
#10114=ORIENTED_EDGE('',*,*,#7793,.T.);
#10115=ORIENTED_EDGE('',*,*,#7797,.F.);
#10116=ORIENTED_EDGE('',*,*,#7796,.T.);
#11505=CYLINDRICAL_SURFACE('',#14696,0.350000000000001);
#11506=CYLINDRICAL_SURFACE('',#14699,0.199999999999999);
#12082=ADVANCED_FACE('',(#2357,#1370),#1717,.T.);
#12083=ADVANCED_FACE('',(#2358),#11505,.T.);
#12084=ADVANCED_FACE('',(#2359),#1718,.F.);
#12085=ADVANCED_FACE('',(#2360),#11506,.T.);
#12086=ADVANCED_FACE('',(#2361),#1719,.T.);
#12458=CLOSED_SHELL('',(#12082,#12083,#12084,#12085,#12086));
#14692=AXIS2_PLACEMENT_3D('',#21723,#17892,#17893);
#14693=AXIS2_PLACEMENT_3D('',#21724,#17894,#17895);
#14694=AXIS2_PLACEMENT_3D('',#21726,#17896,#17897);
#14695=AXIS2_PLACEMENT_3D('',#21728,#17898,#17899);
#14696=AXIS2_PLACEMENT_3D('',#21729,#17900,#17901);
#14697=AXIS2_PLACEMENT_3D('',#21732,#17903,#17904);
#14698=AXIS2_PLACEMENT_3D('',#21733,#17905,#17906);
#14699=AXIS2_PLACEMENT_3D('',#21734,#17907,#17908);
#14700=AXIS2_PLACEMENT_3D('',#21736,#17909,#17910);
#14701=AXIS2_PLACEMENT_3D('',#21738,#17912,#17913);
#17892=DIRECTION('axis',(0.,0.,1.));
#17893=DIRECTION('refdir',(1.,0.,0.));
#17894=DIRECTION('center_axis',(0.,1.,0.));
#17895=DIRECTION('ref_axis',(1.,0.,0.));
#17896=DIRECTION('center_axis',(0.,1.,0.));
#17897=DIRECTION('ref_axis',(1.,0.,0.));
#17898=DIRECTION('center_axis',(0.,1.,0.));
#17899=DIRECTION('ref_axis',(1.,0.,0.));
#17900=DIRECTION('center_axis',(0.,1.,0.));
#17901=DIRECTION('ref_axis',(1.,0.,0.));
#17902=DIRECTION('',(0.,-1.,0.));
#17903=DIRECTION('center_axis',(0.,1.,0.));
#17904=DIRECTION('ref_axis',(1.,0.,0.));
#17905=DIRECTION('center_axis',(0.,1.,0.));
#17906=DIRECTION('ref_axis',(1.,0.,0.));
#17907=DIRECTION('center_axis',(0.,1.,0.));
#17908=DIRECTION('ref_axis',(1.,0.,0.));
#17909=DIRECTION('center_axis',(0.,1.,0.));
#17910=DIRECTION('ref_axis',(1.,0.,0.));
#17911=DIRECTION('',(0.,-1.,0.));
#17912=DIRECTION('center_axis',(0.,1.,0.));
#17913=DIRECTION('ref_axis',(1.,0.,0.));
#21723=CARTESIAN_POINT('',(0.,0.,0.));
#21724=CARTESIAN_POINT('Origin',(22.893930933827,-0.8,27.3496056572921));
#21725=CARTESIAN_POINT('',(22.543930933827,-0.8,27.3496056572921));
#21726=CARTESIAN_POINT('Origin',(22.893930933827,-0.8,27.3496056572921));
#21727=CARTESIAN_POINT('',(22.693930933827,-0.8,27.3496056572921));
#21728=CARTESIAN_POINT('Origin',(22.893930933827,-0.8,27.3496056572921));
#21729=CARTESIAN_POINT('Origin',(22.893930933827,-1.2,27.3496056572921));
#21730=CARTESIAN_POINT('',(22.543930933827,-1.2,27.3496056572921));
#21731=CARTESIAN_POINT('',(22.543930933827,-1.2,27.3496056572921));
#21732=CARTESIAN_POINT('Origin',(22.893930933827,-1.2,27.3496056572921));
#21733=CARTESIAN_POINT('Origin',(22.893930933827,-1.2,27.3496056572921));
#21734=CARTESIAN_POINT('Origin',(22.893930933827,-0.8,27.3496056572921));
#21735=CARTESIAN_POINT('',(22.693930933827,-0.1,27.3496056572921));
#21736=CARTESIAN_POINT('Origin',(22.893930933827,-0.1,27.3496056572921));
#21737=CARTESIAN_POINT('',(22.693930933827,-0.8,27.3496056572921));
#21738=CARTESIAN_POINT('Origin',(22.893930933827,-0.1,27.3496056572921));
#23564=UNCERTAINTY_MEASURE_WITH_UNIT(LENGTH_MEASURE(0.001),#23729,
'DISTANCE_ACCURACY_VALUE',
'Maximum model space distance between geometric entities at asserted c
onnectivities');
#23611=UNCERTAINTY_MEASURE_WITH_UNIT(LENGTH_MEASURE(0.001),#23729,
'DISTANCE_ACCURACY_VALUE',
'Maximum model space distance between geometric entities at asserted c
onnectivities');
#23681=(
GEOMETRIC_REPRESENTATION_CONTEXT(3)
GLOBAL_UNCERTAINTY_ASSIGNED_CONTEXT((#23564))
GLOBAL_UNIT_ASSIGNED_CONTEXT((#23729,#23731,#23732))
REPRESENTATION_CONTEXT('','3D')
);
#23728=(
GEOMETRIC_REPRESENTATION_CONTEXT(3)
GLOBAL_UNCERTAINTY_ASSIGNED_CONTEXT((#23611))
GLOBAL_UNIT_ASSIGNED_CONTEXT((#23729,#23731,#23732))
REPRESENTATION_CONTEXT('','3D')
);
#23729=(
LENGTH_UNIT()
NAMED_UNIT(*)
SI_UNIT(.CENTI.,.METRE.)
);
#23731=(
NAMED_UNIT(*)
PLANE_ANGLE_UNIT()
SI_UNIT($,.RADIAN.)
);
#23732=(
NAMED_UNIT(*)
SI_UNIT($,.STERADIAN.)
SOLID_ANGLE_UNIT()
);
#23802=SHAPE_DEFINITION_REPRESENTATION(#23918,#24181);
#23918=PRODUCT_DEFINITION_SHAPE('',$,#24298);
#24181=SHAPE_REPRESENTATION('',(#14692),#23681);
#24228=PRODUCT_DEFINITION_CONTEXT('part definition',#24578,'design');
#24298=PRODUCT_DEFINITION('M4 short cap screw (26)',
'M4 short cap screw (26)',#24414,#24228);
#24414=PRODUCT_DEFINITION_FORMATION('',$,#24649);
#24578=APPLICATION_CONTEXT(
'Core Data for Automotive Mechanical Design Process');
#24579=PRODUCT_CONTEXT('part definition',#24578,'mechanical');
#24649=PRODUCT('M4 short cap screw (26)','M4 short cap screw (26)',
'M4 short cap screw (26)',(#24579));
#24766=COLOUR_RGB('Black',0.12,0.14,0.17);
#24767=FILL_AREA_STYLE_COLOUR('',#24766);
#24768=FILL_AREA_STYLE('',(#24767));
#24769=SURFACE_STYLE_FILL_AREA(#24768);
#24770=SURFACE_SIDE_STYLE('',(#24769));
#24771=SURFACE_STYLE_USAGE(.BOTH.,#24770);
#24772=PRESENTATION_STYLE_ASSIGNMENT((#24771));
ENDSEC;
END-ISO-10303-21;
